ISO-10303-21;
HEADER;
/* Generated by software containing ST-Developer
 * from STEP Tools, Inc. (www.steptools.com) 
 */

FILE_DESCRIPTION(
/* description */ (''),
/* implementation_level */ '2;1');

FILE_NAME(
/* name */ 'Bracket_04.step',
/* time_stamp */ '2026-10-22T16:03:28+06:00',
/* author */ (''),
/* organization */ (''),
/* preprocessor_version */ 'ST-DEVELOPER v20.2',
/* originating_system */ 'Autodesk Translation Framework v15.15.0.0',
/* authorisation */ '');

FILE_SCHEMA (('AUTOMOTIVE_DESIGN { 1 0 10303 214 3 1 1 }'));
ENDSEC;

DATA;
#10=MECHANICAL_DESIGN_GEOMETRIC_PRESENTATION_REPRESENTATION('',(#94),#6096);
#72=SHAPE_REPRESENTATION_RELATIONSHIP('SRR','None',#6147,#83);
#83=ADVANCED_BREP_SHAPE_REPRESENTATION('',(#105),#6095);
#94=STYLED_ITEM('',(#6234),#105);
#105=MANIFOLD_SOLID_BREP('Bracket_04',#3603);
#150=FACE_BOUND('',#717,.T.);
#151=FACE_BOUND('',#718,.T.);
#152=FACE_BOUND('',#719,.T.);
#153=FACE_BOUND('',#720,.T.);
#154=FACE_BOUND('',#722,.T.);
#155=FACE_BOUND('',#723,.T.);
#156=FACE_BOUND('',#724,.T.);
#157=FACE_BOUND('',#725,.T.);
#286=PLANE('',#4020);
#287=PLANE('',#4021);
#288=PLANE('',#4022);
#289=PLANE('',#4023);
#290=PLANE('',#4024);
#291=PLANE('',#4025);
#292=PLANE('',#4026);
#293=PLANE('',#4027);
#294=PLANE('',#4028);
#295=PLANE('',#4029);
#296=PLANE('',#4030);
#297=PLANE('',#4031);
#470=FACE_OUTER_BOUND('',#702,.T.);
#471=FACE_OUTER_BOUND('',#703,.T.);
#472=FACE_OUTER_BOUND('',#704,.T.);
#473=FACE_OUTER_BOUND('',#705,.T.);
#474=FACE_OUTER_BOUND('',#706,.T.);
#475=FACE_OUTER_BOUND('',#707,.T.);
#476=FACE_OUTER_BOUND('',#708,.T.);
#477=FACE_OUTER_BOUND('',#709,.T.);
#478=FACE_OUTER_BOUND('',#710,.T.);
#479=FACE_OUTER_BOUND('',#711,.T.);
#480=FACE_OUTER_BOUND('',#712,.T.);
#481=FACE_OUTER_BOUND('',#713,.T.);
#482=FACE_OUTER_BOUND('',#714,.T.);
#483=FACE_OUTER_BOUND('',#715,.T.);
#484=FACE_OUTER_BOUND('',#716,.T.);
#485=FACE_OUTER_BOUND('',#721,.T.);
#702=EDGE_LOOP('',(#3280,#3281,#3282,#3283));
#703=EDGE_LOOP('',(#3284,#3285,#3286,#3287));
#704=EDGE_LOOP('',(#3288,#3289,#3290,#3291));
#705=EDGE_LOOP('',(#3292,#3293,#3294,#3295));
#706=EDGE_LOOP('',(#3296,#3297,#3298,#3299));
#707=EDGE_LOOP('',(#3300,#3301,#3302,#3303));
#708=EDGE_LOOP('',(#3304,#3305,#3306,#3307));
#709=EDGE_LOOP('',(#3308,#3309,#3310,#3311));
#710=EDGE_LOOP('',(#3312,#3313,#3314,#3315));
#711=EDGE_LOOP('',(#3316,#3317,#3318,#3319));
#712=EDGE_LOOP('',(#3320,#3321,#3322,#3323));
#713=EDGE_LOOP('',(#3324,#3325,#3326,#3327));
#714=EDGE_LOOP('',(#3328,#3329,#3330,#3331));
#715=EDGE_LOOP('',(#3332,#3333,#3334,#3335));
#716=EDGE_LOOP('',(#3336,#3337,#3338,#3339,#3340,#3341,#3342,#3343,#3344,
#3345));
#717=EDGE_LOOP('',(#3346));
#718=EDGE_LOOP('',(#3347));
#719=EDGE_LOOP('',(#3348));
#720=EDGE_LOOP('',(#3349));
#721=EDGE_LOOP('',(#3350,#3351,#3352,#3353,#3354,#3355,#3356,#3357,#3358,
#3359));
#722=EDGE_LOOP('',(#3360));
#723=EDGE_LOOP('',(#3361));
#724=EDGE_LOOP('',(#3362));
#725=EDGE_LOOP('',(#3363));
#1071=LINE('',#5978,#1450);
#1072=LINE('',#5984,#1451);
#1073=LINE('',#5990,#1452);
#1074=LINE('',#5996,#1453);
#1075=LINE('',#6001,#1454);
#1076=LINE('',#6003,#1455);
#1077=LINE('',#6005,#1456);
#1078=LINE('',#6006,#1457);
#1079=LINE('',#6009,#1458);
#1080=LINE('',#6011,#1459);
#1081=LINE('',#6012,#1460);
#1082=LINE('',#6015,#1461);
#1083=LINE('',#6017,#1462);
#1084=LINE('',#6018,#1463);
#1085=LINE('',#6021,#1464);
#1086=LINE('',#6023,#1465);
#1087=LINE('',#6024,#1466);
#1088=LINE('',#6027,#1467);
#1089=LINE('',#6029,#1468);
#1090=LINE('',#6030,#1469);
#1091=LINE('',#6033,#1470);
#1092=LINE('',#6035,#1471);
#1093=LINE('',#6036,#1472);
#1094=LINE('',#6039,#1473);
#1095=LINE('',#6041,#1474);
#1096=LINE('',#6042,#1475);
#1097=LINE('',#6045,#1476);
#1098=LINE('',#6047,#1477);
#1099=LINE('',#6048,#1478);
#1100=LINE('',#6051,#1479);
#1101=LINE('',#6053,#1480);
#1102=LINE('',#6054,#1481);
#1103=LINE('',#6056,#1482);
#1104=LINE('',#6057,#1483);
#1450=VECTOR('',#4956,1.99999999999999);
#1451=VECTOR('',#4963,1.99999999999999);
#1452=VECTOR('',#4970,1.99999999999999);
#1453=VECTOR('',#4977,1.99999999999999);
#1454=VECTOR('',#4982,10.);
#1455=VECTOR('',#4983,10.);
#1456=VECTOR('',#4984,10.);
#1457=VECTOR('',#4985,10.);
#1458=VECTOR('',#4988,10.);
#1459=VECTOR('',#4989,10.);
#1460=VECTOR('',#4990,10.);
#1461=VECTOR('',#4993,10.);
#1462=VECTOR('',#4994,10.);
#1463=VECTOR('',#4995,10.);
#1464=VECTOR('',#4998,10.);
#1465=VECTOR('',#4999,10.);
#1466=VECTOR('',#5000,10.);
#1467=VECTOR('',#5003,10.);
#1468=VECTOR('',#5004,10.);
#1469=VECTOR('',#5005,10.);
#1470=VECTOR('',#5008,10.);
#1471=VECTOR('',#5009,10.);
#1472=VECTOR('',#5010,10.);
#1473=VECTOR('',#5013,10.);
#1474=VECTOR('',#5014,10.);
#1475=VECTOR('',#5015,10.);
#1476=VECTOR('',#5018,10.);
#1477=VECTOR('',#5019,10.);
#1478=VECTOR('',#5020,10.);
#1479=VECTOR('',#5023,10.);
#1480=VECTOR('',#5024,10.);
#1481=VECTOR('',#5025,10.);
#1482=VECTOR('',#5028,10.);
#1483=VECTOR('',#5029,10.);
#1582=CIRCLE('',#4009,1.99999999999999);
#1583=CIRCLE('',#4010,1.99999999999999);
#1584=CIRCLE('',#4012,1.99999999999999);
#1585=CIRCLE('',#4013,1.99999999999999);
#1586=CIRCLE('',#4015,1.99999999999999);
#1587=CIRCLE('',#4016,1.99999999999999);
#1588=CIRCLE('',#4018,1.99999999999999);
#1589=CIRCLE('',#4019,1.99999999999999);
#1881=VERTEX_POINT('',#5975);
#1882=VERTEX_POINT('',#5977);
#1883=VERTEX_POINT('',#5981);
#1884=VERTEX_POINT('',#5983);
#1885=VERTEX_POINT('',#5987);
#1886=VERTEX_POINT('',#5989);
#1887=VERTEX_POINT('',#5993);
#1888=VERTEX_POINT('',#5995);
#1889=VERTEX_POINT('',#5999);
#1890=VERTEX_POINT('',#6000);
#1891=VERTEX_POINT('',#6002);
#1892=VERTEX_POINT('',#6004);
#1893=VERTEX_POINT('',#6008);
#1894=VERTEX_POINT('',#6010);
#1895=VERTEX_POINT('',#6014);
#1896=VERTEX_POINT('',#6016);
#1897=VERTEX_POINT('',#6020);
#1898=VERTEX_POINT('',#6022);
#1899=VERTEX_POINT('',#6026);
#1900=VERTEX_POINT('',#6028);
#1901=VERTEX_POINT('',#6032);
#1902=VERTEX_POINT('',#6034);
#1903=VERTEX_POINT('',#6038);
#1904=VERTEX_POINT('',#6040);
#1905=VERTEX_POINT('',#6044);
#1906=VERTEX_POINT('',#6046);
#1907=VERTEX_POINT('',#6050);
#1908=VERTEX_POINT('',#6052);
#2352=EDGE_CURVE('',#1881,#1881,#1582,.T.);
#2353=EDGE_CURVE('',#1881,#1882,#1071,.T.);
#2354=EDGE_CURVE('',#1882,#1882,#1583,.T.);
#2355=EDGE_CURVE('',#1883,#1883,#1584,.T.);
#2356=EDGE_CURVE('',#1883,#1884,#1072,.T.);
#2357=EDGE_CURVE('',#1884,#1884,#1585,.T.);
#2358=EDGE_CURVE('',#1885,#1885,#1586,.T.);
#2359=EDGE_CURVE('',#1885,#1886,#1073,.T.);
#2360=EDGE_CURVE('',#1886,#1886,#1587,.T.);
#2361=EDGE_CURVE('',#1887,#1887,#1588,.T.);
#2362=EDGE_CURVE('',#1887,#1888,#1074,.T.);
#2363=EDGE_CURVE('',#1888,#1888,#1589,.T.);
#2364=EDGE_CURVE('',#1889,#1890,#1075,.T.);
#2365=EDGE_CURVE('',#1890,#1891,#1076,.T.);
#2366=EDGE_CURVE('',#1892,#1891,#1077,.T.);
#2367=EDGE_CURVE('',#1889,#1892,#1078,.T.);
#2368=EDGE_CURVE('',#1893,#1889,#1079,.T.);
#2369=EDGE_CURVE('',#1894,#1892,#1080,.T.);
#2370=EDGE_CURVE('',#1893,#1894,#1081,.T.);
#2371=EDGE_CURVE('',#1895,#1893,#1082,.T.);
#2372=EDGE_CURVE('',#1896,#1894,#1083,.T.);
#2373=EDGE_CURVE('',#1895,#1896,#1084,.T.);
#2374=EDGE_CURVE('',#1897,#1895,#1085,.T.);
#2375=EDGE_CURVE('',#1898,#1896,#1086,.T.);
#2376=EDGE_CURVE('',#1897,#1898,#1087,.T.);
#2377=EDGE_CURVE('',#1899,#1897,#1088,.T.);
#2378=EDGE_CURVE('',#1900,#1898,#1089,.T.);
#2379=EDGE_CURVE('',#1899,#1900,#1090,.T.);
#2380=EDGE_CURVE('',#1901,#1899,#1091,.T.);
#2381=EDGE_CURVE('',#1902,#1900,#1092,.T.);
#2382=EDGE_CURVE('',#1901,#1902,#1093,.T.);
#2383=EDGE_CURVE('',#1903,#1901,#1094,.T.);
#2384=EDGE_CURVE('',#1904,#1902,#1095,.T.);
#2385=EDGE_CURVE('',#1903,#1904,#1096,.T.);
#2386=EDGE_CURVE('',#1905,#1903,#1097,.T.);
#2387=EDGE_CURVE('',#1906,#1904,#1098,.T.);
#2388=EDGE_CURVE('',#1905,#1906,#1099,.T.);
#2389=EDGE_CURVE('',#1907,#1905,#1100,.T.);
#2390=EDGE_CURVE('',#1908,#1906,#1101,.T.);
#2391=EDGE_CURVE('',#1907,#1908,#1102,.T.);
#2392=EDGE_CURVE('',#1890,#1907,#1103,.T.);
#2393=EDGE_CURVE('',#1891,#1908,#1104,.T.);
#3280=ORIENTED_EDGE('',*,*,#2352,.F.);
#3281=ORIENTED_EDGE('',*,*,#2353,.T.);
#3282=ORIENTED_EDGE('',*,*,#2354,.T.);
#3283=ORIENTED_EDGE('',*,*,#2353,.F.);
#3284=ORIENTED_EDGE('',*,*,#2355,.F.);
#3285=ORIENTED_EDGE('',*,*,#2356,.T.);
#3286=ORIENTED_EDGE('',*,*,#2357,.T.);
#3287=ORIENTED_EDGE('',*,*,#2356,.F.);
#3288=ORIENTED_EDGE('',*,*,#2358,.F.);
#3289=ORIENTED_EDGE('',*,*,#2359,.T.);
#3290=ORIENTED_EDGE('',*,*,#2360,.T.);
#3291=ORIENTED_EDGE('',*,*,#2359,.F.);
#3292=ORIENTED_EDGE('',*,*,#2361,.F.);
#3293=ORIENTED_EDGE('',*,*,#2362,.T.);
#3294=ORIENTED_EDGE('',*,*,#2363,.T.);
#3295=ORIENTED_EDGE('',*,*,#2362,.F.);
#3296=ORIENTED_EDGE('',*,*,#2364,.T.);
#3297=ORIENTED_EDGE('',*,*,#2365,.T.);
#3298=ORIENTED_EDGE('',*,*,#2366,.F.);
#3299=ORIENTED_EDGE('',*,*,#2367,.F.);
#3300=ORIENTED_EDGE('',*,*,#2368,.T.);
#3301=ORIENTED_EDGE('',*,*,#2367,.T.);
#3302=ORIENTED_EDGE('',*,*,#2369,.F.);
#3303=ORIENTED_EDGE('',*,*,#2370,.F.);
#3304=ORIENTED_EDGE('',*,*,#2371,.T.);
#3305=ORIENTED_EDGE('',*,*,#2370,.T.);
#3306=ORIENTED_EDGE('',*,*,#2372,.F.);
#3307=ORIENTED_EDGE('',*,*,#2373,.F.);
#3308=ORIENTED_EDGE('',*,*,#2374,.T.);
#3309=ORIENTED_EDGE('',*,*,#2373,.T.);
#3310=ORIENTED_EDGE('',*,*,#2375,.F.);
#3311=ORIENTED_EDGE('',*,*,#2376,.F.);
#3312=ORIENTED_EDGE('',*,*,#2377,.T.);
#3313=ORIENTED_EDGE('',*,*,#2376,.T.);
#3314=ORIENTED_EDGE('',*,*,#2378,.F.);
#3315=ORIENTED_EDGE('',*,*,#2379,.F.);
#3316=ORIENTED_EDGE('',*,*,#2380,.T.);
#3317=ORIENTED_EDGE('',*,*,#2379,.T.);
#3318=ORIENTED_EDGE('',*,*,#2381,.F.);
#3319=ORIENTED_EDGE('',*,*,#2382,.F.);
#3320=ORIENTED_EDGE('',*,*,#2383,.T.);
#3321=ORIENTED_EDGE('',*,*,#2382,.T.);
#3322=ORIENTED_EDGE('',*,*,#2384,.F.);
#3323=ORIENTED_EDGE('',*,*,#2385,.F.);
#3324=ORIENTED_EDGE('',*,*,#2386,.T.);
#3325=ORIENTED_EDGE('',*,*,#2385,.T.);
#3326=ORIENTED_EDGE('',*,*,#2387,.F.);
#3327=ORIENTED_EDGE('',*,*,#2388,.F.);
#3328=ORIENTED_EDGE('',*,*,#2389,.T.);
#3329=ORIENTED_EDGE('',*,*,#2388,.T.);
#3330=ORIENTED_EDGE('',*,*,#2390,.F.);
#3331=ORIENTED_EDGE('',*,*,#2391,.F.);
#3332=ORIENTED_EDGE('',*,*,#2392,.T.);
#3333=ORIENTED_EDGE('',*,*,#2391,.T.);
#3334=ORIENTED_EDGE('',*,*,#2393,.F.);
#3335=ORIENTED_EDGE('',*,*,#2365,.F.);
#3336=ORIENTED_EDGE('',*,*,#2393,.T.);
#3337=ORIENTED_EDGE('',*,*,#2390,.T.);
#3338=ORIENTED_EDGE('',*,*,#2387,.T.);
#3339=ORIENTED_EDGE('',*,*,#2384,.T.);
#3340=ORIENTED_EDGE('',*,*,#2381,.T.);
#3341=ORIENTED_EDGE('',*,*,#2378,.T.);
#3342=ORIENTED_EDGE('',*,*,#2375,.T.);
#3343=ORIENTED_EDGE('',*,*,#2372,.T.);
#3344=ORIENTED_EDGE('',*,*,#2369,.T.);
#3345=ORIENTED_EDGE('',*,*,#2366,.T.);
#3346=ORIENTED_EDGE('',*,*,#2361,.T.);
#3347=ORIENTED_EDGE('',*,*,#2358,.T.);
#3348=ORIENTED_EDGE('',*,*,#2355,.T.);
#3349=ORIENTED_EDGE('',*,*,#2352,.T.);
#3350=ORIENTED_EDGE('',*,*,#2392,.F.);
#3351=ORIENTED_EDGE('',*,*,#2364,.F.);
#3352=ORIENTED_EDGE('',*,*,#2368,.F.);
#3353=ORIENTED_EDGE('',*,*,#2371,.F.);
#3354=ORIENTED_EDGE('',*,*,#2374,.F.);
#3355=ORIENTED_EDGE('',*,*,#2377,.F.);
#3356=ORIENTED_EDGE('',*,*,#2380,.F.);
#3357=ORIENTED_EDGE('',*,*,#2383,.F.);
#3358=ORIENTED_EDGE('',*,*,#2386,.F.);
#3359=ORIENTED_EDGE('',*,*,#2389,.F.);
#3360=ORIENTED_EDGE('',*,*,#2363,.F.);
#3361=ORIENTED_EDGE('',*,*,#2360,.F.);
#3362=ORIENTED_EDGE('',*,*,#2357,.F.);
#3363=ORIENTED_EDGE('',*,*,#2354,.F.);
#3401=CYLINDRICAL_SURFACE('',#4008,1.99999999999999);
#3402=CYLINDRICAL_SURFACE('',#4011,1.99999999999999);
#3403=CYLINDRICAL_SURFACE('',#4014,1.99999999999999);
#3404=CYLINDRICAL_SURFACE('',#4017,1.99999999999999);
#3577=ADVANCED_FACE('',(#470),#3401,.F.);
#3578=ADVANCED_FACE('',(#471),#3402,.F.);
#3579=ADVANCED_FACE('',(#472),#3403,.F.);
#3580=ADVANCED_FACE('',(#473),#3404,.F.);
#3581=ADVANCED_FACE('',(#474),#286,.T.);
#3582=ADVANCED_FACE('',(#475),#287,.T.);
#3583=ADVANCED_FACE('',(#476),#288,.T.);
#3584=ADVANCED_FACE('',(#477),#289,.T.);
#3585=ADVANCED_FACE('',(#478),#290,.T.);
#3586=ADVANCED_FACE('',(#479),#291,.T.);
#3587=ADVANCED_FACE('',(#480),#292,.T.);
#3588=ADVANCED_FACE('',(#481),#293,.T.);
#3589=ADVANCED_FACE('',(#482),#294,.T.);
#3590=ADVANCED_FACE('',(#483),#295,.T.);
#3591=ADVANCED_FACE('',(#484,#150,#151,#152,#153),#296,.T.);
#3592=ADVANCED_FACE('',(#485,#154,#155,#156,#157),#297,.F.);
#3603=CLOSED_SHELL('',(#3577,#3578,#3579,#3580,#3581,#3582,#3583,#3584,
#3585,#3586,#3587,#3588,#3589,#3590,#3591,#3592));
#4007=AXIS2_PLACEMENT_3D('',#5973,#4950,#4951);
#4008=AXIS2_PLACEMENT_3D('',#5974,#4952,#4953);
#4009=AXIS2_PLACEMENT_3D('',#5976,#4954,#4955);
#4010=AXIS2_PLACEMENT_3D('',#5979,#4957,#4958);
#4011=AXIS2_PLACEMENT_3D('',#5980,#4959,#4960);
#4012=AXIS2_PLACEMENT_3D('',#5982,#4961,#4962);
#4013=AXIS2_PLACEMENT_3D('',#5985,#4964,#4965);
#4014=AXIS2_PLACEMENT_3D('',#5986,#4966,#4967);
#4015=AXIS2_PLACEMENT_3D('',#5988,#4968,#4969);
#4016=AXIS2_PLACEMENT_3D('',#5991,#4971,#4972);
#4017=AXIS2_PLACEMENT_3D('',#5992,#4973,#4974);
#4018=AXIS2_PLACEMENT_3D('',#5994,#4975,#4976);
#4019=AXIS2_PLACEMENT_3D('',#5997,#4978,#4979);
#4020=AXIS2_PLACEMENT_3D('',#5998,#4980,#4981);
#4021=AXIS2_PLACEMENT_3D('',#6007,#4986,#4987);
#4022=AXIS2_PLACEMENT_3D('',#6013,#4991,#4992);
#4023=AXIS2_PLACEMENT_3D('',#6019,#4996,#4997);
#4024=AXIS2_PLACEMENT_3D('',#6025,#5001,#5002);
#4025=AXIS2_PLACEMENT_3D('',#6031,#5006,#5007);
#4026=AXIS2_PLACEMENT_3D('',#6037,#5011,#5012);
#4027=AXIS2_PLACEMENT_3D('',#6043,#5016,#5017);
#4028=AXIS2_PLACEMENT_3D('',#6049,#5021,#5022);
#4029=AXIS2_PLACEMENT_3D('',#6055,#5026,#5027);
#4030=AXIS2_PLACEMENT_3D('',#6058,#5030,#5031);
#4031=AXIS2_PLACEMENT_3D('',#6059,#5032,#5033);
#4950=DIRECTION('axis',(0.,0.,1.));
#4951=DIRECTION('refdir',(1.,0.,0.));
#4952=DIRECTION('center_axis',(0.,1.,0.));
#4953=DIRECTION('ref_axis',(-1.,0.,0.));
#4954=DIRECTION('center_axis',(0.,-1.,0.));
#4955=DIRECTION('ref_axis',(-1.,0.,0.));
#4956=DIRECTION('',(0.,-1.,0.));
#4957=DIRECTION('center_axis',(0.,-1.,0.));
#4958=DIRECTION('ref_axis',(-1.,0.,0.));
#4959=DIRECTION('center_axis',(0.,1.,0.));
#4960=DIRECTION('ref_axis',(-1.,0.,0.));
#4961=DIRECTION('center_axis',(0.,-1.,0.));
#4962=DIRECTION('ref_axis',(-1.,0.,0.));
#4963=DIRECTION('',(0.,-1.,0.));
#4964=DIRECTION('center_axis',(0.,-1.,0.));
#4965=DIRECTION('ref_axis',(-1.,0.,0.));
#4966=DIRECTION('center_axis',(0.,1.,0.));
#4967=DIRECTION('ref_axis',(-1.,0.,0.));
#4968=DIRECTION('center_axis',(0.,-1.,0.));
#4969=DIRECTION('ref_axis',(-1.,0.,0.));
#4970=DIRECTION('',(0.,-1.,0.));
#4971=DIRECTION('center_axis',(0.,-1.,0.));
#4972=DIRECTION('ref_axis',(-1.,0.,0.));
#4973=DIRECTION('center_axis',(0.,1.,0.));
#4974=DIRECTION('ref_axis',(-1.,0.,0.));
#4975=DIRECTION('center_axis',(0.,-1.,0.));
#4976=DIRECTION('ref_axis',(-1.,0.,0.));
#4977=DIRECTION('',(0.,-1.,0.));
#4978=DIRECTION('center_axis',(0.,-1.,0.));
#4979=DIRECTION('ref_axis',(-1.,0.,0.));
#4980=DIRECTION('center_axis',(0.,0.,-1.));
#4981=DIRECTION('ref_axis',(-1.,0.,0.));
#4982=DIRECTION('',(-1.,0.,0.));
#4983=DIRECTION('',(0.,1.,0.));
#4984=DIRECTION('',(-1.,0.,0.));
#4985=DIRECTION('',(0.,1.,0.));
#4986=DIRECTION('center_axis',(-1.,0.,0.));
#4987=DIRECTION('ref_axis',(0.,0.,1.));
#4988=DIRECTION('',(0.,0.,1.));
#4989=DIRECTION('',(0.,0.,1.));
#4990=DIRECTION('',(0.,1.,0.));
#4991=DIRECTION('center_axis',(0.,0.,1.));
#4992=DIRECTION('ref_axis',(1.,0.,0.));
#4993=DIRECTION('',(1.,0.,0.));
#4994=DIRECTION('',(1.,0.,0.));
#4995=DIRECTION('',(0.,1.,0.));
#4996=DIRECTION('center_axis',(-1.,0.,0.));
#4997=DIRECTION('ref_axis',(0.,0.,1.));
#4998=DIRECTION('',(0.,0.,1.));
#4999=DIRECTION('',(0.,0.,1.));
#5000=DIRECTION('',(0.,1.,0.));
#5001=DIRECTION('center_axis',(0.,0.,-1.));
#5002=DIRECTION('ref_axis',(-1.,0.,0.));
#5003=DIRECTION('',(-1.,0.,0.));
#5004=DIRECTION('',(-1.,0.,0.));
#5005=DIRECTION('',(0.,1.,0.));
#5006=DIRECTION('center_axis',(1.,0.,0.));
#5007=DIRECTION('ref_axis',(0.,0.,-1.));
#5008=DIRECTION('',(0.,0.,-1.));
#5009=DIRECTION('',(0.,0.,-1.));
#5010=DIRECTION('',(0.,1.,0.));
#5011=DIRECTION('center_axis',(0.,0.,1.));
#5012=DIRECTION('ref_axis',(1.,0.,0.));
#5013=DIRECTION('',(1.,0.,0.));
#5014=DIRECTION('',(1.,0.,0.));
#5015=DIRECTION('',(0.,1.,0.));
#5016=DIRECTION('center_axis',(-1.,0.,0.));
#5017=DIRECTION('ref_axis',(0.,0.,1.));
#5018=DIRECTION('',(0.,0.,1.));
#5019=DIRECTION('',(0.,0.,1.));
#5020=DIRECTION('',(0.,1.,0.));
#5021=DIRECTION('center_axis',(0.,0.,-1.));
#5022=DIRECTION('ref_axis',(-1.,0.,0.));
#5023=DIRECTION('',(-1.,0.,0.));
#5024=DIRECTION('',(-1.,0.,0.));
#5025=DIRECTION('',(0.,1.,0.));
#5026=DIRECTION('center_axis',(1.,0.,0.));
#5027=DIRECTION('ref_axis',(0.,0.,-1.));
#5028=DIRECTION('',(0.,0.,-1.));
#5029=DIRECTION('',(0.,0.,-1.));
#5030=DIRECTION('center_axis',(0.,1.,0.));
#5031=DIRECTION('ref_axis',(-1.,0.,0.));
#5032=DIRECTION('center_axis',(0.,1.,0.));
#5033=DIRECTION('ref_axis',(-1.,0.,0.));
#5973=CARTESIAN_POINT('',(0.,0.,0.));
#5974=CARTESIAN_POINT('Origin',(31.6092837386808,460.5,108.939950998448));
#5975=CARTESIAN_POINT('',(33.6092837386808,463.5,108.939950998448));
#5976=CARTESIAN_POINT('Origin',(31.6092837386808,463.5,108.939950998448));
#5977=CARTESIAN_POINT('',(33.6092837386808,460.5,108.939950998448));
#5978=CARTESIAN_POINT('',(33.6092837386808,460.5,108.939950998448));
#5979=CARTESIAN_POINT('Origin',(31.6092837386808,460.5,108.939950998448));
#5980=CARTESIAN_POINT('Origin',(71.0061608111161,460.5,95.0000000000015));
#5981=CARTESIAN_POINT('',(73.0061608111161,463.5,95.0000000000015));
#5982=CARTESIAN_POINT('Origin',(71.0061608111161,463.5,95.0000000000015));
#5983=CARTESIAN_POINT('',(73.0061608111161,460.5,95.0000000000015));
#5984=CARTESIAN_POINT('',(73.0061608111161,460.5,95.0000000000015));
#5985=CARTESIAN_POINT('Origin',(71.0061608111161,460.5,95.0000000000015));
#5986=CARTESIAN_POINT('Origin',(28.0061608111161,460.5,95.0000000000015));
#5987=CARTESIAN_POINT('',(30.0061608111161,463.5,95.0000000000015));
#5988=CARTESIAN_POINT('Origin',(28.0061608111161,463.5,95.0000000000015));
#5989=CARTESIAN_POINT('',(30.0061608111161,460.5,95.0000000000015));
#5990=CARTESIAN_POINT('',(30.0061608111161,460.5,95.0000000000015));
#5991=CARTESIAN_POINT('Origin',(28.0061608111161,460.5,95.0000000000015));
#5992=CARTESIAN_POINT('Origin',(67.4030378835514,460.5,108.939950998448));
#5993=CARTESIAN_POINT('',(69.4030378835514,463.5,108.939950998448));
#5994=CARTESIAN_POINT('Origin',(67.4030378835514,463.5,108.939950998448));
#5995=CARTESIAN_POINT('',(69.4030378835514,460.5,108.939950998448));
#5996=CARTESIAN_POINT('',(69.4030378835514,460.5,108.939950998448));
#5997=CARTESIAN_POINT('Origin',(67.4030378835514,460.5,108.939950998448));
#5998=CARTESIAN_POINT('Origin',(67.5061608111161,460.5,105.000000000001));
#5999=CARTESIAN_POINT('',(67.5061608111161,460.5,105.000000000001));
#6000=CARTESIAN_POINT('',(31.5061608111161,460.5,105.000000000001));
#6001=CARTESIAN_POINT('',(67.5061608111161,460.5,105.000000000001));
#6002=CARTESIAN_POINT('',(31.5061608111161,463.5,105.000000000001));
#6003=CARTESIAN_POINT('',(31.5061608111161,460.5,105.000000000001));
#6004=CARTESIAN_POINT('',(67.5061608111161,463.5,105.000000000001));
#6005=CARTESIAN_POINT('',(67.5061608111161,463.5,105.000000000001));
#6006=CARTESIAN_POINT('',(67.5061608111161,460.5,105.000000000001));
#6007=CARTESIAN_POINT('Origin',(67.5061608111161,460.5,85.0000000000015));
#6008=CARTESIAN_POINT('',(67.5061608111161,460.5,85.0000000000015));
#6009=CARTESIAN_POINT('',(67.5061608111161,460.5,85.0000000000015));
#6010=CARTESIAN_POINT('',(67.5061608111161,463.5,85.0000000000015));
#6011=CARTESIAN_POINT('',(67.5061608111161,463.5,85.0000000000015));
#6012=CARTESIAN_POINT('',(67.5061608111161,460.5,85.0000000000015));
#6013=CARTESIAN_POINT('Origin',(51.5061608111161,460.5,85.0000000000015));
#6014=CARTESIAN_POINT('',(51.5061608111161,460.5,85.0000000000015));
#6015=CARTESIAN_POINT('',(31.5061608111161,460.5,85.0000000000015));
#6016=CARTESIAN_POINT('',(51.5061608111161,463.5,85.0000000000015));
#6017=CARTESIAN_POINT('',(31.5061608111161,463.5,85.0000000000015));
#6018=CARTESIAN_POINT('',(51.5061608111161,460.5,85.0000000000015));
#6019=CARTESIAN_POINT('Origin',(51.5061608111161,460.5,77.5000000000015));
#6020=CARTESIAN_POINT('',(51.5061608111161,460.5,77.5000000000015));
#6021=CARTESIAN_POINT('',(51.5061608111161,460.5,65.0000000000015));
#6022=CARTESIAN_POINT('',(51.5061608111161,463.5,77.5000000000015));
#6023=CARTESIAN_POINT('',(51.5061608111161,463.5,65.0000000000015));
#6024=CARTESIAN_POINT('',(51.5061608111161,460.5,77.5000000000015));
#6025=CARTESIAN_POINT('Origin',(74.5061608111161,460.5,77.5000000000015));
#6026=CARTESIAN_POINT('',(74.5061608111161,460.5,77.5000000000015));
#6027=CARTESIAN_POINT('',(74.5061608111161,460.5,77.5000000000015));
#6028=CARTESIAN_POINT('',(74.5061608111161,463.5,77.5000000000015));
#6029=CARTESIAN_POINT('',(74.5061608111161,463.5,77.5000000000015));
#6030=CARTESIAN_POINT('',(74.5061608111161,460.5,77.5000000000015));
#6031=CARTESIAN_POINT('Origin',(74.5061608111161,460.5,112.500000000001));
#6032=CARTESIAN_POINT('',(74.5061608111161,460.5,112.500000000001));
#6033=CARTESIAN_POINT('',(74.5061608111161,460.5,112.500000000001));
#6034=CARTESIAN_POINT('',(74.5061608111161,463.5,112.500000000001));
#6035=CARTESIAN_POINT('',(74.5061608111161,463.5,112.500000000001));
#6036=CARTESIAN_POINT('',(74.5061608111161,460.5,112.500000000001));
#6037=CARTESIAN_POINT('Origin',(24.5061608111161,460.5,112.500000000001));
#6038=CARTESIAN_POINT('',(24.5061608111161,460.5,112.500000000001));
#6039=CARTESIAN_POINT('',(24.5061608111161,460.5,112.500000000001));
#6040=CARTESIAN_POINT('',(24.5061608111161,463.5,112.500000000001));
#6041=CARTESIAN_POINT('',(24.5061608111161,463.5,112.500000000001));
#6042=CARTESIAN_POINT('',(24.5061608111161,460.5,112.500000000001));
#6043=CARTESIAN_POINT('Origin',(24.5061608111161,460.5,77.5000000000015));
#6044=CARTESIAN_POINT('',(24.5061608111161,460.5,77.5000000000015));
#6045=CARTESIAN_POINT('',(24.5061608111161,460.5,77.5000000000015));
#6046=CARTESIAN_POINT('',(24.5061608111161,463.5,77.5000000000015));
#6047=CARTESIAN_POINT('',(24.5061608111161,463.5,77.5000000000015));
#6048=CARTESIAN_POINT('',(24.5061608111161,460.5,77.5000000000015));
#6049=CARTESIAN_POINT('Origin',(31.5061608111161,460.5,77.5000000000015));
#6050=CARTESIAN_POINT('',(31.5061608111161,460.5,77.5000000000015));
#6051=CARTESIAN_POINT('',(74.5061608111161,460.5,77.5000000000015));
#6052=CARTESIAN_POINT('',(31.5061608111161,463.5,77.5000000000015));
#6053=CARTESIAN_POINT('',(74.5061608111161,463.5,77.5000000000015));
#6054=CARTESIAN_POINT('',(31.5061608111161,460.5,77.5000000000015));
#6055=CARTESIAN_POINT('Origin',(31.5061608111161,460.5,105.000000000001));
#6056=CARTESIAN_POINT('',(31.5061608111161,460.5,85.0000000000015));
#6057=CARTESIAN_POINT('',(31.5061608111161,463.5,85.0000000000015));
#6058=CARTESIAN_POINT('Origin',(49.5061608111161,463.5,95.0000000000015));
#6059=CARTESIAN_POINT('Origin',(49.5061608111161,460.5,95.0000000000015));
#6082=UNCERTAINTY_MEASURE_WITH_UNIT(LENGTH_MEASURE(0.01),#6097,
'DISTANCE_ACCURACY_VALUE',
'Maximum model space distance between geometric entities at asserted c
onnectivities');
#6083=UNCERTAINTY_MEASURE_WITH_UNIT(LENGTH_MEASURE(0.01),#6097,
'DISTANCE_ACCURACY_VALUE',
'Maximum model space distance between geometric entities at asserted c
onnectivities');
#6095=(
GEOMETRIC_REPRESENTATION_CONTEXT(3)
GLOBAL_UNCERTAINTY_ASSIGNED_CONTEXT((#6082))
GLOBAL_UNIT_ASSIGNED_CONTEXT((#6097,#6099,#6100))
REPRESENTATION_CONTEXT('','3D')
);
#6096=(
GEOMETRIC_REPRESENTATION_CONTEXT(3)
GLOBAL_UNCERTAINTY_ASSIGNED_CONTEXT((#6083))
GLOBAL_UNIT_ASSIGNED_CONTEXT((#6097,#6099,#6100))
REPRESENTATION_CONTEXT('','3D')
);
#6097=(
LENGTH_UNIT()
NAMED_UNIT(*)
SI_UNIT(.MILLI.,.METRE.)
);
#6099=(
NAMED_UNIT(*)
PLANE_ANGLE_UNIT()
SI_UNIT($,.RADIAN.)
);
#6100=(
NAMED_UNIT(*)
SI_UNIT($,.STERADIAN.)
SOLID_ANGLE_UNIT()
);
#6112=SHAPE_DEFINITION_REPRESENTATION(#6124,#6147);
#6124=PRODUCT_DEFINITION_SHAPE('',$,#6160);
#6147=SHAPE_REPRESENTATION('',(#4007),#6095);
#6148=PRODUCT_DEFINITION_CONTEXT('part definition',#6186,'design');
#6160=PRODUCT_DEFINITION('Bracket_04','Bracket_04',#6172,#6148);
#6172=PRODUCT_DEFINITION_FORMATION('',$,#6199);
#6186=APPLICATION_CONTEXT(
'Core Data for Automotive Mechanical Design Process');
#6187=PRODUCT_CONTEXT('part definition',#6186,'mechanical');
#6199=PRODUCT('Bracket_04','Bracket_04',$,(#6187));
#6228=COLOUR_RGB('Dark Blue',0.08,0.2,0.34);
#6229=FILL_AREA_STYLE_COLOUR('',#6228);
#6230=FILL_AREA_STYLE('',(#6229));
#6231=SURFACE_STYLE_FILL_AREA(#6230);
#6232=SURFACE_SIDE_STYLE('',(#6231));
#6233=SURFACE_STYLE_USAGE(.BOTH.,#6232);
#6234=PRESENTATION_STYLE_ASSIGNMENT((#6233));
ENDSEC;
END-ISO-10303-21;
